ISO-10303-21;
HEADER;
/* Generated by software containing ST-Developer
 * from STEP Tools, Inc. (www.steptools.com) 
 */

FILE_DESCRIPTION(
/* description */ ('Counter shaft with two pulleys and keyed hub'),
/* implementation_level */ '2;1');

FILE_NAME(
/* name */ 'M8x25 Bolt.step',
/* time_stamp */ '2026-10-27T10:46:10-07:00',
/* author */ (''),
/* organization */ (''),
/* preprocessor_version */ 'ST-DEVELOPER v20.2',
/* originating_system */ 'Autodesk Translation Framework v15.17.0.0',
/* authorisation */ '');

FILE_SCHEMA (('AUTOMOTIVE_DESIGN { 1 0 10303 214 3 1 1 }'));
ENDSEC;

DATA;
#10=MECHANICAL_DESIGN_GEOMETRIC_PRESENTATION_REPRESENTATION('',(#301),#10821);
#11=CONICAL_SURFACE('',#6042,0.625,0.785398163397448);
#12=CONICAL_SURFACE('',#6046,0.635,0.785398163397449);
#13=CONICAL_SURFACE('',#6050,0.41,0.463647609000806);
#20=ORIENTED_CLOSED_SHELL('',*,#5584,.F.);
#22=BREP_WITH_VOIDS('Body1',#5585,(#20));
#250=SHAPE_REPRESENTATION_RELATIONSHIP('SRR','None',#10937,#275);
#275=ADVANCED_BREP_SHAPE_REPRESENTATION('',(#22),#10805);
#301=STYLED_ITEM('',(#11142),#22);
#387=FACE_BOUND('',#1046,.T.);
#483=PLANE('',#6030);
#484=PLANE('',#6031);
#485=PLANE('',#6032);
#486=PLANE('',#6033);
#487=PLANE('',#6034);
#488=PLANE('',#6035);
#489=PLANE('',#6036);
#490=PLANE('',#6037);
#491=PLANE('',#6038);
#492=PLANE('',#6040);
#493=PLANE('',#6048);
#671=FACE_OUTER_BOUND('',#1032,.T.);
#672=FACE_OUTER_BOUND('',#1033,.T.);
#673=FACE_OUTER_BOUND('',#1034,.T.);
#674=FACE_OUTER_BOUND('',#1035,.T.);
#675=FACE_OUTER_BOUND('',#1036,.T.);
#676=FACE_OUTER_BOUND('',#1037,.T.);
#677=FACE_OUTER_BOUND('',#1038,.T.);
#678=FACE_OUTER_BOUND('',#1039,.T.);
#679=FACE_OUTER_BOUND('',#1040,.T.);
#680=FACE_OUTER_BOUND('',#1041,.T.);
#681=FACE_OUTER_BOUND('',#1042,.T.);
#682=FACE_OUTER_BOUND('',#1043,.T.);
#683=FACE_OUTER_BOUND('',#1044,.T.);
#684=FACE_OUTER_BOUND('',#1045,.T.);
#685=FACE_OUTER_BOUND('',#1047,.T.);
#686=FACE_OUTER_BOUND('',#1048,.T.);
#1032=EDGE_LOOP('',(#3997,#3998,#3999,#4000));
#1033=EDGE_LOOP('',(#4001,#4002,#4003,#4004));
#1034=EDGE_LOOP('',(#4005,#4006,#4007,#4008));
#1035=EDGE_LOOP('',(#4009,#4010,#4011,#4012));
#1036=EDGE_LOOP('',(#4013,#4014,#4015,#4016));
#1037=EDGE_LOOP('',(#4017,#4018,#4019,#4020));
#1038=EDGE_LOOP('',(#4021,#4022,#4023,#4024,#4025,#4026));
#1039=EDGE_LOOP('',(#4027,#4028,#4029,#4030,#4031,#4032));
#1040=EDGE_LOOP('',(#4033));
#1041=EDGE_LOOP('',(#4034));
#1042=EDGE_LOOP('',(#4035,#4036,#4037,#4038));
#1043=EDGE_LOOP('',(#4039,#4040,#4041,#4042));
#1044=EDGE_LOOP('',(#4043,#4044,#4045,#4046));
#1045=EDGE_LOOP('',(#4047));
#1046=EDGE_LOOP('',(#4048));
#1047=EDGE_LOOP('',(#4049,#4050,#4051,#4052));
#1048=EDGE_LOOP('',(#4053,#4054,#4055,#4056));
#1413=LINE('',#9136,#1802);
#1414=LINE('',#9138,#1803);
#1415=LINE('',#9140,#1804);
#1416=LINE('',#9141,#1805);
#1417=LINE('',#9144,#1806);
#1418=LINE('',#9146,#1807);
#1419=LINE('',#9147,#1808);
#1420=LINE('',#9150,#1809);
#1421=LINE('',#9152,#1810);
#1422=LINE('',#9153,#1811);
#1423=LINE('',#9156,#1812);
#1424=LINE('',#9158,#1813);
#1425=LINE('',#9159,#1814);
#1426=LINE('',#9162,#1815);
#1427=LINE('',#9164,#1816);
#1428=LINE('',#9165,#1817);
#1429=LINE('',#9167,#1818);
#1430=LINE('',#9168,#1819);
#1431=LINE('',#9180,#1820);
#1432=LINE('',#9184,#1821);
#1433=LINE('',#9188,#1822);
#1434=LINE('',#9195,#1823);
#1435=LINE('',#9197,#1824);
#1802=VECTOR('',#6973,1.);
#1803=VECTOR('',#6974,1.);
#1804=VECTOR('',#6975,1.);
#1805=VECTOR('',#6976,1.);
#1806=VECTOR('',#6979,1.);
#1807=VECTOR('',#6980,1.);
#1808=VECTOR('',#6981,1.);
#1809=VECTOR('',#6984,1.);
#1810=VECTOR('',#6985,1.);
#1811=VECTOR('',#6986,1.);
#1812=VECTOR('',#6989,1.);
#1813=VECTOR('',#6990,1.);
#1814=VECTOR('',#6991,1.);
#1815=VECTOR('',#6994,1.);
#1816=VECTOR('',#6995,1.);
#1817=VECTOR('',#6996,1.);
#1818=VECTOR('',#6999,1.);
#1819=VECTOR('',#7000,1.);
#1820=VECTOR('',#7017,0.625);
#1821=VECTOR('',#7022,0.65);
#1822=VECTOR('',#7027,0.635);
#1823=VECTOR('',#7036,0.41);
#1824=VECTOR('',#7039,0.4);
#2139=CIRCLE('',#6039,0.3933);
#2140=CIRCLE('',#6041,0.6);
#2141=CIRCLE('',#6043,0.65);
#2142=CIRCLE('',#6045,0.65);
#2143=CIRCLE('',#6047,0.62);
#2144=CIRCLE('',#6049,0.42);
#2145=CIRCLE('',#6051,0.3933);
#2514=VERTEX_POINT('',#9134);
#2515=VERTEX_POINT('',#9135);
#2516=VERTEX_POINT('',#9137);
#2517=VERTEX_POINT('',#9139);
#2518=VERTEX_POINT('',#9143);
#2519=VERTEX_POINT('',#9145);
#2520=VERTEX_POINT('',#9149);
#2521=VERTEX_POINT('',#9151);
#2522=VERTEX_POINT('',#9155);
#2523=VERTEX_POINT('',#9157);
#2524=VERTEX_POINT('',#9161);
#2525=VERTEX_POINT('',#9163);
#2526=VERTEX_POINT('',#9172);
#2527=VERTEX_POINT('',#9175);
#2528=VERTEX_POINT('',#9178);
#2529=VERTEX_POINT('',#9182);
#2530=VERTEX_POINT('',#9186);
#2531=VERTEX_POINT('',#9190);
#2532=VERTEX_POINT('',#9193);
#3071=EDGE_CURVE('',#2514,#2515,#1413,.T.);
#3072=EDGE_CURVE('',#2515,#2516,#1414,.T.);
#3073=EDGE_CURVE('',#2516,#2517,#1415,.T.);
#3074=EDGE_CURVE('',#2514,#2517,#1416,.T.);
#3075=EDGE_CURVE('',#2515,#2518,#1417,.T.);
#3076=EDGE_CURVE('',#2518,#2519,#1418,.T.);
#3077=EDGE_CURVE('',#2519,#2516,#1419,.T.);
#3078=EDGE_CURVE('',#2518,#2520,#1420,.T.);
#3079=EDGE_CURVE('',#2520,#2521,#1421,.T.);
#3080=EDGE_CURVE('',#2521,#2519,#1422,.T.);
#3081=EDGE_CURVE('',#2520,#2522,#1423,.T.);
#3082=EDGE_CURVE('',#2522,#2523,#1424,.T.);
#3083=EDGE_CURVE('',#2523,#2521,#1425,.T.);
#3084=EDGE_CURVE('',#2522,#2524,#1426,.T.);
#3085=EDGE_CURVE('',#2524,#2525,#1427,.T.);
#3086=EDGE_CURVE('',#2525,#2523,#1428,.T.);
#3087=EDGE_CURVE('',#2524,#2514,#1429,.T.);
#3088=EDGE_CURVE('',#2517,#2525,#1430,.T.);
#3089=EDGE_CURVE('',#2526,#2526,#2139,.T.);
#3090=EDGE_CURVE('',#2527,#2527,#2140,.T.);
#3091=EDGE_CURVE('',#2528,#2528,#2141,.T.);
#3092=EDGE_CURVE('',#2528,#2527,#1431,.T.);
#3093=EDGE_CURVE('',#2529,#2529,#2142,.T.);
#3094=EDGE_CURVE('',#2529,#2528,#1432,.T.);
#3095=EDGE_CURVE('',#2530,#2530,#2143,.T.);
#3096=EDGE_CURVE('',#2530,#2529,#1433,.T.);
#3097=EDGE_CURVE('',#2531,#2531,#2144,.T.);
#3098=EDGE_CURVE('',#2532,#2532,#2145,.F.);
#3099=EDGE_CURVE('',#2532,#2531,#1434,.T.);
#3100=EDGE_CURVE('',#2526,#2532,#1435,.T.);
#3997=ORIENTED_EDGE('',*,*,#3071,.T.);
#3998=ORIENTED_EDGE('',*,*,#3072,.T.);
#3999=ORIENTED_EDGE('',*,*,#3073,.T.);
#4000=ORIENTED_EDGE('',*,*,#3074,.F.);
#4001=ORIENTED_EDGE('',*,*,#3075,.T.);
#4002=ORIENTED_EDGE('',*,*,#3076,.T.);
#4003=ORIENTED_EDGE('',*,*,#3077,.T.);
#4004=ORIENTED_EDGE('',*,*,#3072,.F.);
#4005=ORIENTED_EDGE('',*,*,#3078,.T.);
#4006=ORIENTED_EDGE('',*,*,#3079,.T.);
#4007=ORIENTED_EDGE('',*,*,#3080,.T.);
#4008=ORIENTED_EDGE('',*,*,#3076,.F.);
#4009=ORIENTED_EDGE('',*,*,#3081,.T.);
#4010=ORIENTED_EDGE('',*,*,#3082,.T.);
#4011=ORIENTED_EDGE('',*,*,#3083,.T.);
#4012=ORIENTED_EDGE('',*,*,#3079,.F.);
#4013=ORIENTED_EDGE('',*,*,#3084,.T.);
#4014=ORIENTED_EDGE('',*,*,#3085,.T.);
#4015=ORIENTED_EDGE('',*,*,#3086,.T.);
#4016=ORIENTED_EDGE('',*,*,#3082,.F.);
#4017=ORIENTED_EDGE('',*,*,#3087,.T.);
#4018=ORIENTED_EDGE('',*,*,#3074,.T.);
#4019=ORIENTED_EDGE('',*,*,#3088,.T.);
#4020=ORIENTED_EDGE('',*,*,#3085,.F.);
#4021=ORIENTED_EDGE('',*,*,#3087,.F.);
#4022=ORIENTED_EDGE('',*,*,#3084,.F.);
#4023=ORIENTED_EDGE('',*,*,#3081,.F.);
#4024=ORIENTED_EDGE('',*,*,#3078,.F.);
#4025=ORIENTED_EDGE('',*,*,#3075,.F.);
#4026=ORIENTED_EDGE('',*,*,#3071,.F.);
#4027=ORIENTED_EDGE('',*,*,#3088,.F.);
#4028=ORIENTED_EDGE('',*,*,#3073,.F.);
#4029=ORIENTED_EDGE('',*,*,#3077,.F.);
#4030=ORIENTED_EDGE('',*,*,#3080,.F.);
#4031=ORIENTED_EDGE('',*,*,#3083,.F.);
#4032=ORIENTED_EDGE('',*,*,#3086,.F.);
#4033=ORIENTED_EDGE('',*,*,#3089,.F.);
#4034=ORIENTED_EDGE('',*,*,#3090,.F.);
#4035=ORIENTED_EDGE('',*,*,#3091,.F.);
#4036=ORIENTED_EDGE('',*,*,#3092,.T.);
#4037=ORIENTED_EDGE('',*,*,#3090,.T.);
#4038=ORIENTED_EDGE('',*,*,#3092,.F.);
#4039=ORIENTED_EDGE('',*,*,#3093,.F.);
#4040=ORIENTED_EDGE('',*,*,#3094,.T.);
#4041=ORIENTED_EDGE('',*,*,#3091,.T.);
#4042=ORIENTED_EDGE('',*,*,#3094,.F.);
#4043=ORIENTED_EDGE('',*,*,#3095,.F.);
#4044=ORIENTED_EDGE('',*,*,#3096,.T.);
#4045=ORIENTED_EDGE('',*,*,#3093,.T.);
#4046=ORIENTED_EDGE('',*,*,#3096,.F.);
#4047=ORIENTED_EDGE('',*,*,#3095,.T.);
#4048=ORIENTED_EDGE('',*,*,#3097,.F.);
#4049=ORIENTED_EDGE('',*,*,#3098,.F.);
#4050=ORIENTED_EDGE('',*,*,#3099,.T.);
#4051=ORIENTED_EDGE('',*,*,#3097,.T.);
#4052=ORIENTED_EDGE('',*,*,#3099,.F.);
#4053=ORIENTED_EDGE('',*,*,#3089,.T.);
#4054=ORIENTED_EDGE('',*,*,#3100,.T.);
#4055=ORIENTED_EDGE('',*,*,#3098,.T.);
#4056=ORIENTED_EDGE('',*,*,#3100,.F.);
#5142=CYLINDRICAL_SURFACE('',#6044,0.65);
#5143=CYLINDRICAL_SURFACE('',#6052,0.3933);
#5342=ADVANCED_FACE('',(#671),#483,.F.);
#5343=ADVANCED_FACE('',(#672),#484,.F.);
#5344=ADVANCED_FACE('',(#673),#485,.F.);
#5345=ADVANCED_FACE('',(#674),#486,.F.);
#5346=ADVANCED_FACE('',(#675),#487,.F.);
#5347=ADVANCED_FACE('',(#676),#488,.F.);
#5348=ADVANCED_FACE('',(#677),#489,.F.);
#5349=ADVANCED_FACE('',(#678),#490,.F.);
#5350=ADVANCED_FACE('',(#679),#491,.F.);
#5351=ADVANCED_FACE('',(#680),#492,.T.);
#5352=ADVANCED_FACE('',(#681),#11,.T.);
#5353=ADVANCED_FACE('',(#682),#5142,.T.);
#5354=ADVANCED_FACE('',(#683),#12,.T.);
#5355=ADVANCED_FACE('',(#684,#387),#493,.T.);
#5356=ADVANCED_FACE('',(#685),#13,.T.);
#5357=ADVANCED_FACE('',(#686),#5143,.T.);
#5584=CLOSED_SHELL('',(#5342,#5343,#5344,#5345,#5346,#5347,#5348,#5349));
#5585=CLOSED_SHELL('',(#5350,#5351,#5352,#5353,#5354,#5355,#5356,#5357));
#6029=AXIS2_PLACEMENT_3D('',#9132,#6969,#6970);
#6030=AXIS2_PLACEMENT_3D('',#9133,#6971,#6972);
#6031=AXIS2_PLACEMENT_3D('',#9142,#6977,#6978);
#6032=AXIS2_PLACEMENT_3D('',#9148,#6982,#6983);
#6033=AXIS2_PLACEMENT_3D('',#9154,#6987,#6988);
#6034=AXIS2_PLACEMENT_3D('',#9160,#6992,#6993);
#6035=AXIS2_PLACEMENT_3D('',#9166,#6997,#6998);
#6036=AXIS2_PLACEMENT_3D('',#9169,#7001,#7002);
#6037=AXIS2_PLACEMENT_3D('',#9170,#7003,#7004);
#6038=AXIS2_PLACEMENT_3D('',#9171,#7005,#7006);
#6039=AXIS2_PLACEMENT_3D('',#9173,#7007,#7008);
#6040=AXIS2_PLACEMENT_3D('',#9174,#7009,#7010);
#6041=AXIS2_PLACEMENT_3D('',#9176,#7011,#7012);
#6042=AXIS2_PLACEMENT_3D('',#9177,#7013,#7014);
#6043=AXIS2_PLACEMENT_3D('',#9179,#7015,#7016);
#6044=AXIS2_PLACEMENT_3D('',#9181,#7018,#7019);
#6045=AXIS2_PLACEMENT_3D('',#9183,#7020,#7021);
#6046=AXIS2_PLACEMENT_3D('',#9185,#7023,#7024);
#6047=AXIS2_PLACEMENT_3D('',#9187,#7025,#7026);
#6048=AXIS2_PLACEMENT_3D('',#9189,#7028,#7029);
#6049=AXIS2_PLACEMENT_3D('',#9191,#7030,#7031);
#6050=AXIS2_PLACEMENT_3D('',#9192,#7032,#7033);
#6051=AXIS2_PLACEMENT_3D('',#9194,#7034,#7035);
#6052=AXIS2_PLACEMENT_3D('',#9196,#7037,#7038);
#6969=DIRECTION('axis',(0.,0.,1.));
#6970=DIRECTION('refdir',(1.,0.,0.));
#6971=DIRECTION('center_axis',(0.866025403784439,0.,-0.5));
#6972=DIRECTION('ref_axis',(0.5,0.,0.866025403784439));
#6973=DIRECTION('',(-0.5,0.,-0.866025403784439));
#6974=DIRECTION('',(0.,-1.,0.));
#6975=DIRECTION('',(0.5,0.,0.866025403784439));
#6976=DIRECTION('',(0.,-1.,0.));
#6977=DIRECTION('center_axis',(1.60246890531964E-16,0.,-1.));
#6978=DIRECTION('ref_axis',(1.,0.,1.60246890531964E-16));
#6979=DIRECTION('',(-1.,0.,-1.60246890531964E-16));
#6980=DIRECTION('',(0.,-1.,0.));
#6981=DIRECTION('',(1.,0.,1.60246890531964E-16));
#6982=DIRECTION('center_axis',(-0.866025403784439,0.,-0.5));
#6983=DIRECTION('ref_axis',(0.5,0.,-0.866025403784439));
#6984=DIRECTION('',(-0.5,0.,0.866025403784439));
#6985=DIRECTION('',(0.,-1.,0.));
#6986=DIRECTION('',(0.5,0.,-0.866025403784439));
#6987=DIRECTION('center_axis',(-0.866025403784439,0.,0.5));
#6988=DIRECTION('ref_axis',(-0.5,0.,-0.866025403784439));
#6989=DIRECTION('',(0.5,0.,0.866025403784439));
#6990=DIRECTION('',(0.,-1.,0.));
#6991=DIRECTION('',(-0.5,0.,-0.866025403784439));
#6992=DIRECTION('center_axis',(-1.60246890531964E-16,0.,1.));
#6993=DIRECTION('ref_axis',(-1.,0.,-1.60246890531964E-16));
#6994=DIRECTION('',(1.,0.,1.60246890531964E-16));
#6995=DIRECTION('',(0.,-1.,0.));
#6996=DIRECTION('',(-1.,0.,-1.60246890531964E-16));
#6997=DIRECTION('center_axis',(0.866025403784439,0.,0.5));
#6998=DIRECTION('ref_axis',(-0.5,0.,0.866025403784439));
#6999=DIRECTION('',(0.5,0.,-0.866025403784439));
#7000=DIRECTION('',(-0.5,0.,0.866025403784439));
#7001=DIRECTION('center_axis',(0.,1.,0.));
#7002=DIRECTION('ref_axis',(1.,0.,0.));
#7003=DIRECTION('center_axis',(0.,-1.,0.));
#7004=DIRECTION('ref_axis',(0.,0.,-1.));
#7005=DIRECTION('center_axis',(0.,1.,0.));
#7006=DIRECTION('ref_axis',(1.,0.,0.));
#7007=DIRECTION('center_axis',(0.,1.,0.));
#7008=DIRECTION('ref_axis',(1.,0.,0.));
#7009=DIRECTION('center_axis',(0.,1.,0.));
#7010=DIRECTION('ref_axis',(0.,0.,1.));
#7011=DIRECTION('center_axis',(0.,-1.,0.));
#7012=DIRECTION('ref_axis',(1.,0.,0.));
#7013=DIRECTION('center_axis',(0.,-1.,0.));
#7014=DIRECTION('ref_axis',(1.,0.,0.));
#7015=DIRECTION('center_axis',(0.,-1.,0.));
#7016=DIRECTION('ref_axis',(1.,0.,0.));
#7017=DIRECTION('',(0.707106781186548,0.707106781186547,8.65956056235493E-17));
#7018=DIRECTION('center_axis',(0.,-1.,0.));
#7019=DIRECTION('ref_axis',(1.,0.,0.));
#7020=DIRECTION('center_axis',(0.,-1.,0.));
#7021=DIRECTION('ref_axis',(1.,0.,0.));
#7022=DIRECTION('',(0.,1.,0.));
#7023=DIRECTION('center_axis',(0.,1.,0.));
#7024=DIRECTION('ref_axis',(1.,0.,0.));
#7025=DIRECTION('center_axis',(0.,-1.,0.));
#7026=DIRECTION('ref_axis',(1.,0.,0.));
#7027=DIRECTION('',(-0.707106781186548,0.707106781186547,-8.65956056235494E-17));
#7028=DIRECTION('center_axis',(0.,-1.,0.));
#7029=DIRECTION('ref_axis',(0.,0.,-1.));
#7030=DIRECTION('center_axis',(0.,-1.,0.));
#7031=DIRECTION('ref_axis',(1.,0.,0.));
#7032=DIRECTION('center_axis',(0.,1.,0.));
#7033=DIRECTION('ref_axis',(1.,0.,0.));
#7034=DIRECTION('center_axis',(0.,1.,0.));
#7035=DIRECTION('ref_axis',(1.,0.,0.));
#7036=DIRECTION('',(-0.447213595499958,0.894427190999916,-5.47678698264203E-17));
#7037=DIRECTION('center_axis',(0.,-1.,0.));
#7038=DIRECTION('ref_axis',(1.,0.,0.));
#7039=DIRECTION('',(0.,1.,0.));
#9132=CARTESIAN_POINT('',(0.,0.,0.));
#9133=CARTESIAN_POINT('Origin',(0.173205080756888,-0.8,-0.3));
#9134=CARTESIAN_POINT('',(0.346410161513775,-0.8,0.));
#9135=CARTESIAN_POINT('',(0.173205080756888,-0.8,-0.3));
#9136=CARTESIAN_POINT('',(0.346410161513775,-0.8,0.));
#9137=CARTESIAN_POINT('',(0.173205080756888,-1.28,-0.3));
#9138=CARTESIAN_POINT('',(0.173205080756888,-0.8,-0.3));
#9139=CARTESIAN_POINT('',(0.346410161513775,-1.28,0.));
#9140=CARTESIAN_POINT('',(0.346410161513775,-1.28,0.));
#9141=CARTESIAN_POINT('',(0.346410161513775,-0.8,0.));
#9142=CARTESIAN_POINT('Origin',(-0.173205080756888,-0.8,-0.3));
#9143=CARTESIAN_POINT('',(-0.173205080756888,-0.8,-0.3));
#9144=CARTESIAN_POINT('',(0.173205080756888,-0.8,-0.3));
#9145=CARTESIAN_POINT('',(-0.173205080756888,-1.28,-0.3));
#9146=CARTESIAN_POINT('',(-0.173205080756888,-0.8,-0.3));
#9147=CARTESIAN_POINT('',(0.173205080756888,-1.28,-0.3));
#9148=CARTESIAN_POINT('Origin',(-0.346410161513775,-0.8,-5.55111512312578E-17));
#9149=CARTESIAN_POINT('',(-0.346410161513775,-0.8,-4.24230095489963E-17));
#9150=CARTESIAN_POINT('',(-0.173205080756888,-0.8,-0.3));
#9151=CARTESIAN_POINT('',(-0.346410161513775,-1.28,-5.55111512312578E-17));
#9152=CARTESIAN_POINT('',(-0.346410161513775,-0.8,-4.24230095489963E-17));
#9153=CARTESIAN_POINT('',(-0.173205080756888,-1.28,-0.3));
#9154=CARTESIAN_POINT('Origin',(-0.173205080756888,-0.8,0.3));
#9155=CARTESIAN_POINT('',(-0.173205080756888,-0.8,0.3));
#9156=CARTESIAN_POINT('',(-0.346410161513775,-0.8,-4.24230095489963E-17));
#9157=CARTESIAN_POINT('',(-0.173205080756888,-1.28,0.3));
#9158=CARTESIAN_POINT('',(-0.173205080756888,-0.8,0.3));
#9159=CARTESIAN_POINT('',(-0.346410161513775,-1.28,-4.24230095489963E-17));
#9160=CARTESIAN_POINT('Origin',(0.173205080756888,-0.8,0.3));
#9161=CARTESIAN_POINT('',(0.173205080756888,-0.8,0.3));
#9162=CARTESIAN_POINT('',(-0.173205080756888,-0.8,0.3));
#9163=CARTESIAN_POINT('',(0.173205080756888,-1.28,0.3));
#9164=CARTESIAN_POINT('',(0.173205080756888,-0.8,0.3));
#9165=CARTESIAN_POINT('',(-0.173205080756888,-1.28,0.3));
#9166=CARTESIAN_POINT('Origin',(0.346410161513775,-0.8,0.));
#9167=CARTESIAN_POINT('',(0.173205080756888,-0.8,0.3));
#9168=CARTESIAN_POINT('',(0.173205080756888,-1.28,0.3));
#9169=CARTESIAN_POINT('Origin',(0.,-0.8,-5.55111512312578E-17));
#9170=CARTESIAN_POINT('Origin',(0.,-1.28,-5.55111512312578E-17));
#9171=CARTESIAN_POINT('Origin',(0.,-2.5,0.));
#9172=CARTESIAN_POINT('',(-0.3933,-2.5,4.81653586104654E-17));
#9173=CARTESIAN_POINT('Origin',(0.,-2.5,0.));
#9174=CARTESIAN_POINT('Origin',(0.6,0.8,0.));
#9175=CARTESIAN_POINT('',(-0.6,0.8,-7.34788079488412E-17));
#9176=CARTESIAN_POINT('Origin',(0.,0.8,0.));
#9177=CARTESIAN_POINT('Origin',(0.,0.775,0.));
#9178=CARTESIAN_POINT('',(-0.65,0.75,-7.9602041944578E-17));
#9179=CARTESIAN_POINT('Origin',(0.,0.75,0.));
#9180=CARTESIAN_POINT('',(-0.625,0.775,-7.65404249467096E-17));
#9181=CARTESIAN_POINT('Origin',(0.,0.39,0.));
#9182=CARTESIAN_POINT('',(-0.65,0.0299999999999998,-7.9602041944578E-17));
#9183=CARTESIAN_POINT('Origin',(0.,0.0299999999999998,0.));
#9184=CARTESIAN_POINT('',(-0.65,0.39,-7.9602041944578E-17));
#9185=CARTESIAN_POINT('Origin',(0.,0.0150000000000001,0.));
#9186=CARTESIAN_POINT('',(-0.62,5.89805981832114E-17,-7.59281015471359E-17));
#9187=CARTESIAN_POINT('Origin',(0.,0.,0.));
#9188=CARTESIAN_POINT('',(-0.635,0.0150000000000001,-7.77650717458569E-17));
#9189=CARTESIAN_POINT('Origin',(0.42,0.,0.));
#9190=CARTESIAN_POINT('',(-0.42,-3.46944695195361E-18,-5.14351655641888E-17));
#9191=CARTESIAN_POINT('Origin',(0.,0.,0.));
#9192=CARTESIAN_POINT('Origin',(0.,-0.02,0.));
#9193=CARTESIAN_POINT('',(-0.3933,-0.0534000000000001,4.81653586104654E-17));
#9194=CARTESIAN_POINT('Origin',(0.,-0.0534000000000001,0.));
#9195=CARTESIAN_POINT('',(-0.41,-0.02,-5.02105187650415E-17));
#9196=CARTESIAN_POINT('Origin',(0.,-1.48,0.));
#9197=CARTESIAN_POINT('',(-0.3933,-1.48,-4.81653586104654E-17));
#10775=UNCERTAINTY_MEASURE_WITH_UNIT(LENGTH_MEASURE(0.001),#10822,
'DISTANCE_ACCURACY_VALUE',
'Maximum model space distance between geometric entities at asserted c
onnectivities');
#10791=UNCERTAINTY_MEASURE_WITH_UNIT(LENGTH_MEASURE(0.001),#10822,
'DISTANCE_ACCURACY_VALUE',
'Maximum model space distance between geometric entities at asserted c
onnectivities');
#10805=(
GEOMETRIC_REPRESENTATION_CONTEXT(3)
GLOBAL_UNCERTAINTY_ASSIGNED_CONTEXT((#10775))
GLOBAL_UNIT_ASSIGNED_CONTEXT((#10822,#10824,#10825))
REPRESENTATION_CONTEXT('','3D')
);
#10821=(
GEOMETRIC_REPRESENTATION_CONTEXT(3)
GLOBAL_UNCERTAINTY_ASSIGNED_CONTEXT((#10791))
GLOBAL_UNIT_ASSIGNED_CONTEXT((#10822,#10824,#10825))
REPRESENTATION_CONTEXT('','3D')
);
#10822=(
LENGTH_UNIT()
NAMED_UNIT(*)
SI_UNIT(.CENTI.,.METRE.)
);
#10824=(
NAMED_UNIT(*)
PLANE_ANGLE_UNIT()
SI_UNIT($,.RADIAN.)
);
#10825=(
NAMED_UNIT(*)
SI_UNIT($,.STERADIAN.)
SOLID_ANGLE_UNIT()
);
#10839=SHAPE_DEFINITION_REPRESENTATION(#10870,#10937);
#10870=PRODUCT_DEFINITION_SHAPE('',$,#10967);
#10937=SHAPE_REPRESENTATION('',(#6029),#10805);
#10953=PRODUCT_DEFINITION_CONTEXT('part definition',#11042,'design');
#10967=PRODUCT_DEFINITION('M8x25 Bolt','M8x25 Bolt',#10996,#10953);
#10996=PRODUCT_DEFINITION_FORMATION('',$,#11057);
#11042=APPLICATION_CONTEXT(
'Core Data for Automotive Mechanical Design Process');
#11043=PRODUCT_CONTEXT('part definition',#11042,'mechanical');
#11057=PRODUCT('M8x25 Bolt','M8x25 Bolt','M8x25 Bolt',(#11043));
#11136=COLOUR_RGB('Black',0.12,0.14,0.17);
#11137=FILL_AREA_STYLE_COLOUR('',#11136);
#11138=FILL_AREA_STYLE('',(#11137));
#11139=SURFACE_STYLE_FILL_AREA(#11138);
#11140=SURFACE_SIDE_STYLE('',(#11139));
#11141=SURFACE_STYLE_USAGE(.BOTH.,#11140);
#11142=PRESENTATION_STYLE_ASSIGNMENT((#11141));
ENDSEC;
END-ISO-10303-21;
